ISO-10303-21;
HEADER;
/* Generated by software containing ST-Developer
 * from STEP Tools, Inc. (www.steptools.com) 
 */

FILE_DESCRIPTION(
/* description */ ('Independent 1:2 reduction pantograph. 120 mm parallelogram sides; fix
ed fulcrum on the extension of a 240 mm link. Drawing point halfway al
ong its link, so its XY displacement is one half of the tracing point.
 Replaceable pivot bushes and retained pins. Calibration and productio
n accuracy unassigned.'),
/* implementation_level */ '2;1');

FILE_NAME(
/* name */ 'Pivot washer.step',
/* time_stamp */ '2026-11-07T22:11:57-08:00',
/* author */ (''),
/* organization */ (''),
/* preprocessor_version */ 'ST-DEVELOPER v20.2',
/* originating_system */ 'Autodesk Translation Framework v15.17.0.0',
/* authorisation */ '');

FILE_SCHEMA (('AUTOMOTIVE_DESIGN { 1 0 10303 214 3 1 1 }'));
ENDSEC;

DATA;
#10=MECHANICAL_DESIGN_GEOMETRIC_PRESENTATION_REPRESENTATION('',(#196),#2926);
#170=SHAPE_REPRESENTATION_RELATIONSHIP('SRR','None',#3007,#183);
#183=ADVANCED_BREP_SHAPE_REPRESENTATION('',(#209),#2923);
#196=STYLED_ITEM('',(#3079),#209);
#209=MANIFOLD_SOLID_BREP('Body1',#1551);
#256=FACE_BOUND('',#523,.T.);
#257=FACE_BOUND('',#525,.T.);
#298=PLANE('',#1873);
#299=PLANE('',#1874);
#384=FACE_OUTER_BOUND('',#520,.T.);
#385=FACE_OUTER_BOUND('',#521,.T.);
#386=FACE_OUTER_BOUND('',#522,.T.);
#387=FACE_OUTER_BOUND('',#524,.T.);
#520=EDGE_LOOP('',(#1361,#1362,#1363,#1364));
#521=EDGE_LOOP('',(#1365,#1366,#1367,#1368));
#522=EDGE_LOOP('',(#1369));
#523=EDGE_LOOP('',(#1370));
#524=EDGE_LOOP('',(#1371));
#525=EDGE_LOOP('',(#1372));
#604=LINE('',#2812,#685);
#605=LINE('',#2818,#686);
#685=VECTOR('',#2340,5.);
#686=VECTOR('',#2347,10.);
#775=CIRCLE('',#1868,5.);
#776=CIRCLE('',#1869,5.);
#777=CIRCLE('',#1871,10.);
#778=CIRCLE('',#1872,10.);
#883=VERTEX_POINT('',#2809);
#884=VERTEX_POINT('',#2811);
#885=VERTEX_POINT('',#2815);
#886=VERTEX_POINT('',#2817);
#1045=EDGE_CURVE('',#883,#883,#775,.T.);
#1046=EDGE_CURVE('',#883,#884,#604,.T.);
#1047=EDGE_CURVE('',#884,#884,#776,.T.);
#1048=EDGE_CURVE('',#885,#885,#777,.T.);
#1049=EDGE_CURVE('',#885,#886,#605,.T.);
#1050=EDGE_CURVE('',#886,#886,#778,.T.);
#1361=ORIENTED_EDGE('',*,*,#1045,.F.);
#1362=ORIENTED_EDGE('',*,*,#1046,.T.);
#1363=ORIENTED_EDGE('',*,*,#1047,.T.);
#1364=ORIENTED_EDGE('',*,*,#1046,.F.);
#1365=ORIENTED_EDGE('',*,*,#1048,.F.);
#1366=ORIENTED_EDGE('',*,*,#1049,.T.);
#1367=ORIENTED_EDGE('',*,*,#1050,.T.);
#1368=ORIENTED_EDGE('',*,*,#1049,.F.);
#1369=ORIENTED_EDGE('',*,*,#1048,.T.);
#1370=ORIENTED_EDGE('',*,*,#1045,.T.);
#1371=ORIENTED_EDGE('',*,*,#1050,.F.);
#1372=ORIENTED_EDGE('',*,*,#1047,.F.);
#1444=CYLINDRICAL_SURFACE('',#1867,5.);
#1445=CYLINDRICAL_SURFACE('',#1870,10.);
#1528=ADVANCED_FACE('',(#384),#1444,.F.);
#1529=ADVANCED_FACE('',(#385),#1445,.T.);
#1530=ADVANCED_FACE('',(#386,#256),#298,.T.);
#1531=ADVANCED_FACE('',(#387,#257),#299,.F.);
#1551=CLOSED_SHELL('',(#1528,#1529,#1530,#1531));
#1866=AXIS2_PLACEMENT_3D('',#2807,#2334,#2335);
#1867=AXIS2_PLACEMENT_3D('',#2808,#2336,#2337);
#1868=AXIS2_PLACEMENT_3D('',#2810,#2338,#2339);
#1869=AXIS2_PLACEMENT_3D('',#2813,#2341,#2342);
#1870=AXIS2_PLACEMENT_3D('',#2814,#2343,#2344);
#1871=AXIS2_PLACEMENT_3D('',#2816,#2345,#2346);
#1872=AXIS2_PLACEMENT_3D('',#2819,#2348,#2349);
#1873=AXIS2_PLACEMENT_3D('',#2820,#2350,#2351);
#1874=AXIS2_PLACEMENT_3D('',#2821,#2352,#2353);
#2334=DIRECTION('axis',(0.,0.,1.));
#2335=DIRECTION('refdir',(1.,0.,0.));
#2336=DIRECTION('center_axis',(0.,0.,1.));
#2337=DIRECTION('ref_axis',(1.,0.,0.));
#2338=DIRECTION('center_axis',(0.,0.,-1.));
#2339=DIRECTION('ref_axis',(1.,0.,0.));
#2340=DIRECTION('',(0.,0.,-1.));
#2341=DIRECTION('center_axis',(0.,0.,-1.));
#2342=DIRECTION('ref_axis',(1.,0.,0.));
#2343=DIRECTION('center_axis',(0.,0.,1.));
#2344=DIRECTION('ref_axis',(1.,0.,0.));
#2345=DIRECTION('center_axis',(0.,0.,1.));
#2346=DIRECTION('ref_axis',(1.,0.,0.));
#2347=DIRECTION('',(0.,0.,-1.));
#2348=DIRECTION('center_axis',(0.,0.,1.));
#2349=DIRECTION('ref_axis',(1.,0.,0.));
#2350=DIRECTION('center_axis',(0.,0.,1.));
#2351=DIRECTION('ref_axis',(1.,0.,0.));
#2352=DIRECTION('center_axis',(0.,0.,1.));
#2353=DIRECTION('ref_axis',(1.,0.,0.));
#2807=CARTESIAN_POINT('',(0.,0.,0.));
#2808=CARTESIAN_POINT('Origin',(0.,0.,0.));
#2809=CARTESIAN_POINT('',(-5.,-6.12323399573677E-16,2.));
#2810=CARTESIAN_POINT('Origin',(0.,0.,2.));
#2811=CARTESIAN_POINT('',(-5.,-6.12323399573677E-16,0.));
#2812=CARTESIAN_POINT('',(-5.,-6.12323399573677E-16,0.));
#2813=CARTESIAN_POINT('Origin',(0.,0.,0.));
#2814=CARTESIAN_POINT('Origin',(0.,0.,0.));
#2815=CARTESIAN_POINT('',(-10.,-1.22464679914735E-15,2.));
#2816=CARTESIAN_POINT('Origin',(0.,0.,2.));
#2817=CARTESIAN_POINT('',(-10.,-1.22464679914735E-15,0.));
#2818=CARTESIAN_POINT('',(-10.,-1.22464679914735E-15,0.));
#2819=CARTESIAN_POINT('Origin',(0.,0.,0.));
#2820=CARTESIAN_POINT('Origin',(0.,0.,2.));
#2821=CARTESIAN_POINT('Origin',(0.,0.,0.));
#2908=UNCERTAINTY_MEASURE_WITH_UNIT(LENGTH_MEASURE(0.01),#2927,
'DISTANCE_ACCURACY_VALUE',
'Maximum model space distance between geometric entities at asserted c
onnectivities');
#2911=UNCERTAINTY_MEASURE_WITH_UNIT(LENGTH_MEASURE(0.01),#2927,
'DISTANCE_ACCURACY_VALUE',
'Maximum model space distance between geometric entities at asserted c
onnectivities');
#2923=(
GEOMETRIC_REPRESENTATION_CONTEXT(3)
GLOBAL_UNCERTAINTY_ASSIGNED_CONTEXT((#2908))
GLOBAL_UNIT_ASSIGNED_CONTEXT((#2927,#2929,#2930))
REPRESENTATION_CONTEXT('','3D')
);
#2926=(
GEOMETRIC_REPRESENTATION_CONTEXT(3)
GLOBAL_UNCERTAINTY_ASSIGNED_CONTEXT((#2911))
GLOBAL_UNIT_ASSIGNED_CONTEXT((#2927,#2929,#2930))
REPRESENTATION_CONTEXT('','3D')
);
#2927=(
LENGTH_UNIT()
NAMED_UNIT(*)
SI_UNIT(.MILLI.,.METRE.)
);
#2929=(
NAMED_UNIT(*)
PLANE_ANGLE_UNIT()
SI_UNIT($,.RADIAN.)
);
#2930=(
NAMED_UNIT(*)
SI_UNIT($,.STERADIAN.)
SOLID_ANGLE_UNIT()
);
#2942=SHAPE_DEFINITION_REPRESENTATION(#2956,#3007);
#2956=PRODUCT_DEFINITION_SHAPE('',$,#3022);
#3007=SHAPE_REPRESENTATION('',(#1866),#2923);
#3010=PRODUCT_DEFINITION_CONTEXT('part definition',#3054,'design');
#3022=PRODUCT_DEFINITION('Pivot washer','Pivot washer',#3036,#3010);
#3036=PRODUCT_DEFINITION_FORMATION('',$,#3067);
#3054=APPLICATION_CONTEXT(
'Core Data for Automotive Mechanical Design Process');
#3055=PRODUCT_CONTEXT('part definition',#3054,'mechanical');
#3067=PRODUCT('Pivot washer','Pivot washer',$,(#3055));
#3079=PRESENTATION_STYLE_ASSIGNMENT((#3091));
#3091=SURFACE_STYLE_USAGE(.BOTH.,#3103);
#3103=SURFACE_SIDE_STYLE('',(#3115));
#3115=SURFACE_STYLE_FILL_AREA(#3127);
#3127=FILL_AREA_STYLE('Washer light gray',(#3139));
#3139=FILL_AREA_STYLE_COLOUR('Washer light gray',#3151);
#3151=COLOUR_RGB('Washer light gray',0.725490196078431,0.752941176470588,
0.792156862745098);
ENDSEC;
END-ISO-10303-21;
